ISO-10303-21;
HEADER;
/* Generated by software containing ST-Developer
 * from STEP Tools, Inc. (www.steptools.com) 
 */

FILE_DESCRIPTION(
/* description */ ('Independent hinged machine back cover with retained hinge pins, perim
eter gasket and quarter-turn cam latch. Nominal cover 360 x 260 x 3 mm
, frame 430 x 300 x 20 mm. No guarding, structural or ingress rating a
ssigned.'),
/* implementation_level */ '2;1');

FILE_NAME(
/* name */ 'Flat washer M6.step',
/* time_stamp */ '2026-11-09T19:36:59-08:00',
/* author */ (''),
/* organization */ (''),
/* preprocessor_version */ 'ST-DEVELOPER v20.2',
/* originating_system */ 'Autodesk Translation Framework v15.17.0.0',
/* authorisation */ '');

FILE_SCHEMA (('AUTOMOTIVE_DESIGN { 1 0 10303 214 3 1 1 }'));
ENDSEC;

DATA;
#10=MECHANICAL_DESIGN_GEOMETRIC_PRESENTATION_REPRESENTATION('',(#214),#32627);
#178=SHAPE_REPRESENTATION_RELATIONSHIP('SRR','None',#32724,#196);
#196=ADVANCED_BREP_SHAPE_REPRESENTATION('',(#232),#32625);
#214=STYLED_ITEM('',(#32812),#232);
#232=MANIFOLD_SOLID_BREP('Body1',#8691);
#289=FACE_BOUND('',#1434,.T.);
#290=FACE_BOUND('',#1436,.T.);
#442=PLANE('',#9465);
#443=PLANE('',#9466);
#901=FACE_OUTER_BOUND('',#1431,.T.);
#902=FACE_OUTER_BOUND('',#1432,.T.);
#903=FACE_OUTER_BOUND('',#1433,.T.);
#904=FACE_OUTER_BOUND('',#1435,.T.);
#1431=EDGE_LOOP('',(#7755,#7756,#7757,#7758));
#1432=EDGE_LOOP('',(#7759,#7760,#7761,#7762));
#1433=EDGE_LOOP('',(#7763));
#1434=EDGE_LOOP('',(#7764));
#1435=EDGE_LOOP('',(#7765));
#1436=EDGE_LOOP('',(#7766));
#1577=CIRCLE('',#9460,3.5);
#1578=CIRCLE('',#9461,3.5);
#1579=CIRCLE('',#9463,7.);
#1580=CIRCLE('',#9464,7.);
#2691=LINE('',#31444,#3237);
#2692=LINE('',#31450,#3238);
#3237=VECTOR('',#11183,3.5);
#3238=VECTOR('',#11190,7.);
#4063=VERTEX_POINT('',#31441);
#4064=VERTEX_POINT('',#31443);
#4065=VERTEX_POINT('',#31447);
#4066=VERTEX_POINT('',#31449);
#5301=EDGE_CURVE('',#4063,#4063,#1577,.T.);
#5302=EDGE_CURVE('',#4063,#4064,#2691,.T.);
#5303=EDGE_CURVE('',#4064,#4064,#1578,.T.);
#5304=EDGE_CURVE('',#4065,#4065,#1579,.T.);
#5305=EDGE_CURVE('',#4065,#4066,#2692,.T.);
#5306=EDGE_CURVE('',#4066,#4066,#1580,.T.);
#7755=ORIENTED_EDGE('',*,*,#5301,.F.);
#7756=ORIENTED_EDGE('',*,*,#5302,.T.);
#7757=ORIENTED_EDGE('',*,*,#5303,.T.);
#7758=ORIENTED_EDGE('',*,*,#5302,.F.);
#7759=ORIENTED_EDGE('',*,*,#5304,.F.);
#7760=ORIENTED_EDGE('',*,*,#5305,.T.);
#7761=ORIENTED_EDGE('',*,*,#5306,.T.);
#7762=ORIENTED_EDGE('',*,*,#5305,.F.);
#7763=ORIENTED_EDGE('',*,*,#5304,.T.);
#7764=ORIENTED_EDGE('',*,*,#5301,.T.);
#7765=ORIENTED_EDGE('',*,*,#5306,.F.);
#7766=ORIENTED_EDGE('',*,*,#5303,.F.);
#8186=CYLINDRICAL_SURFACE('',#9459,3.5);
#8187=CYLINDRICAL_SURFACE('',#9462,7.);
#8649=ADVANCED_FACE('',(#901),#8186,.F.);
#8650=ADVANCED_FACE('',(#902),#8187,.T.);
#8651=ADVANCED_FACE('',(#903,#289),#442,.T.);
#8652=ADVANCED_FACE('',(#904,#290),#443,.F.);
#8691=CLOSED_SHELL('',(#8649,#8650,#8651,#8652));
#9458=AXIS2_PLACEMENT_3D('',#31439,#11177,#11178);
#9459=AXIS2_PLACEMENT_3D('',#31440,#11179,#11180);
#9460=AXIS2_PLACEMENT_3D('',#31442,#11181,#11182);
#9461=AXIS2_PLACEMENT_3D('',#31445,#11184,#11185);
#9462=AXIS2_PLACEMENT_3D('',#31446,#11186,#11187);
#9463=AXIS2_PLACEMENT_3D('',#31448,#11188,#11189);
#9464=AXIS2_PLACEMENT_3D('',#31451,#11191,#11192);
#9465=AXIS2_PLACEMENT_3D('',#31452,#11193,#11194);
#9466=AXIS2_PLACEMENT_3D('',#31453,#11195,#11196);
#11177=DIRECTION('axis',(0.,0.,1.));
#11178=DIRECTION('refdir',(1.,0.,0.));
#11179=DIRECTION('center_axis',(0.,0.,1.));
#11180=DIRECTION('ref_axis',(1.,0.,0.));
#11181=DIRECTION('center_axis',(0.,0.,-1.));
#11182=DIRECTION('ref_axis',(1.,0.,0.));
#11183=DIRECTION('',(0.,0.,-1.));
#11184=DIRECTION('center_axis',(0.,0.,-1.));
#11185=DIRECTION('ref_axis',(1.,0.,0.));
#11186=DIRECTION('center_axis',(0.,0.,1.));
#11187=DIRECTION('ref_axis',(1.,0.,0.));
#11188=DIRECTION('center_axis',(0.,0.,1.));
#11189=DIRECTION('ref_axis',(1.,0.,0.));
#11190=DIRECTION('',(0.,0.,-1.));
#11191=DIRECTION('center_axis',(0.,0.,1.));
#11192=DIRECTION('ref_axis',(1.,0.,0.));
#11193=DIRECTION('center_axis',(0.,0.,1.));
#11194=DIRECTION('ref_axis',(1.,0.,0.));
#11195=DIRECTION('center_axis',(0.,0.,1.));
#11196=DIRECTION('ref_axis',(1.,0.,0.));
#31439=CARTESIAN_POINT('',(0.,0.,0.));
#31440=CARTESIAN_POINT('Origin',(0.,0.,0.));
#31441=CARTESIAN_POINT('',(-3.5,-4.28626379701574E-16,1.));
#31442=CARTESIAN_POINT('Origin',(0.,0.,1.));
#31443=CARTESIAN_POINT('',(-3.5,-4.28626379701574E-16,0.));
#31444=CARTESIAN_POINT('',(-3.5,-4.28626379701574E-16,0.));
#31445=CARTESIAN_POINT('Origin',(0.,0.,0.));
#31446=CARTESIAN_POINT('Origin',(0.,0.,0.));
#31447=CARTESIAN_POINT('',(-7.,-8.57252759403147E-16,1.));
#31448=CARTESIAN_POINT('Origin',(0.,0.,1.));
#31449=CARTESIAN_POINT('',(-7.,-8.57252759403147E-16,0.));
#31450=CARTESIAN_POINT('',(-7.,-8.57252759403147E-16,0.));
#31451=CARTESIAN_POINT('Origin',(0.,0.,0.));
#31452=CARTESIAN_POINT('Origin',(0.,0.,1.));
#31453=CARTESIAN_POINT('Origin',(0.,0.,0.));
#32605=UNCERTAINTY_MEASURE_WITH_UNIT(LENGTH_MEASURE(0.01),#32628,
'DISTANCE_ACCURACY_VALUE',
'Maximum model space distance between geometric entities at asserted c
onnectivities');
#32607=UNCERTAINTY_MEASURE_WITH_UNIT(LENGTH_MEASURE(0.01),#32628,
'DISTANCE_ACCURACY_VALUE',
'Maximum model space distance between geometric entities at asserted c
onnectivities');
#32625=(
GEOMETRIC_REPRESENTATION_CONTEXT(3)
GLOBAL_UNCERTAINTY_ASSIGNED_CONTEXT((#32605))
GLOBAL_UNIT_ASSIGNED_CONTEXT((#32628,#32630,#32631))
REPRESENTATION_CONTEXT('','3D')
);
#32627=(
GEOMETRIC_REPRESENTATION_CONTEXT(3)
GLOBAL_UNCERTAINTY_ASSIGNED_CONTEXT((#32607))
GLOBAL_UNIT_ASSIGNED_CONTEXT((#32628,#32630,#32631))
REPRESENTATION_CONTEXT('','3D')
);
#32628=(
LENGTH_UNIT()
NAMED_UNIT(*)
SI_UNIT(.MILLI.,.METRE.)
);
#32630=(
NAMED_UNIT(*)
PLANE_ANGLE_UNIT()
SI_UNIT($,.RADIAN.)
);
#32631=(
NAMED_UNIT(*)
SI_UNIT($,.STERADIAN.)
SOLID_ANGLE_UNIT()
);
#32649=SHAPE_DEFINITION_REPRESENTATION(#32668,#32724);
#32668=PRODUCT_DEFINITION_SHAPE('',$,#32744);
#32724=SHAPE_REPRESENTATION('',(#9458),#32625);
#32726=PRODUCT_DEFINITION_CONTEXT('part definition',#32785,'design');
#32744=PRODUCT_DEFINITION('Flat washer M6','Flat washer M6',#32763,#32726);
#32763=PRODUCT_DEFINITION_FORMATION('',$,#32804);
#32785=APPLICATION_CONTEXT(
'Core Data for Automotive Mechanical Design Process');
#32786=PRODUCT_CONTEXT('part definition',#32785,'mechanical');
#32804=PRODUCT('Flat washer M6','Flat washer M6',$,(#32786));
#32812=PRESENTATION_STYLE_ASSIGNMENT((#32819));
#32819=SURFACE_STYLE_USAGE(.BOTH.,#32826);
#32826=SURFACE_SIDE_STYLE('',(#32833));
#32833=SURFACE_STYLE_FILL_AREA(#32840);
#32840=FILL_AREA_STYLE('Light gray',(#32847));
#32847=FILL_AREA_STYLE_COLOUR('Light gray',#32854);
#32854=COLOUR_RGB('Light gray',0.725490196078431,0.752941176470588,0.792156862745098);
ENDSEC;
END-ISO-10303-21;
